ISO-10303-21;
HEADER;
/* Generated by software containing ST-Developer
 * from STEP Tools, Inc. (www.steptools.com) 
 */

FILE_DESCRIPTION(
/* description */ ('Cable chain and bracket set'),
/* implementation_level */ '2;1');

FILE_NAME(
/* name */ 'Flat Washer - M6__PD6071.step',
/* time_stamp */ '2026-10-29T17:19:47-07:00',
/* author */ (''),
/* organization */ (''),
/* preprocessor_version */ 'ST-DEVELOPER v20.2',
/* originating_system */ 'Autodesk Translation Framework v15.17.0.0',
/* authorisation */ '');

FILE_SCHEMA (('AUTOMOTIVE_DESIGN { 1 0 10303 214 3 1 1 }'));
ENDSEC;

DATA;
#10=MECHANICAL_DESIGN_GEOMETRIC_PRESENTATION_REPRESENTATION('',(#342),#5929);
#316=SHAPE_REPRESENTATION_RELATIONSHIP('SRR','None',#6047,#329);
#329=ADVANCED_BREP_SHAPE_REPRESENTATION('',(#355),#5914);
#342=STYLED_ITEM('',(#6227),#355);
#355=MANIFOLD_SOLID_BREP('Body1',#3336);
#381=FACE_BOUND('',#808,.T.);
#382=FACE_BOUND('',#810,.T.);
#457=PLANE('',#3573);
#458=PLANE('',#3574);
#605=FACE_OUTER_BOUND('',#805,.T.);
#606=FACE_OUTER_BOUND('',#806,.T.);
#607=FACE_OUTER_BOUND('',#807,.T.);
#608=FACE_OUTER_BOUND('',#809,.T.);
#805=EDGE_LOOP('',(#2617,#2618,#2619,#2620));
#806=EDGE_LOOP('',(#2621,#2622,#2623,#2624));
#807=EDGE_LOOP('',(#2625));
#808=EDGE_LOOP('',(#2626));
#809=EDGE_LOOP('',(#2627));
#810=EDGE_LOOP('',(#2628));
#1053=LINE('',#5259,#1313);
#1054=LINE('',#5265,#1314);
#1313=VECTOR('',#4228,0.320000000000037);
#1314=VECTOR('',#4235,0.600000000000068);
#1501=CIRCLE('',#3568,0.320000000000037);
#1502=CIRCLE('',#3569,0.320000000000037);
#1503=CIRCLE('',#3571,0.600000000000069);
#1504=CIRCLE('',#3572,0.600000000000069);
#1675=VERTEX_POINT('',#5256);
#1676=VERTEX_POINT('',#5258);
#1677=VERTEX_POINT('',#5262);
#1678=VERTEX_POINT('',#5264);
#2009=EDGE_CURVE('',#1675,#1675,#1501,.T.);
#2010=EDGE_CURVE('',#1675,#1676,#1053,.T.);
#2011=EDGE_CURVE('',#1676,#1676,#1502,.T.);
#2012=EDGE_CURVE('',#1677,#1677,#1503,.T.);
#2013=EDGE_CURVE('',#1677,#1678,#1054,.T.);
#2014=EDGE_CURVE('',#1678,#1678,#1504,.T.);
#2617=ORIENTED_EDGE('',*,*,#2009,.F.);
#2618=ORIENTED_EDGE('',*,*,#2010,.T.);
#2619=ORIENTED_EDGE('',*,*,#2011,.T.);
#2620=ORIENTED_EDGE('',*,*,#2010,.F.);
#2621=ORIENTED_EDGE('',*,*,#2012,.F.);
#2622=ORIENTED_EDGE('',*,*,#2013,.T.);
#2623=ORIENTED_EDGE('',*,*,#2014,.T.);
#2624=ORIENTED_EDGE('',*,*,#2013,.F.);
#2625=ORIENTED_EDGE('',*,*,#2012,.T.);
#2626=ORIENTED_EDGE('',*,*,#2009,.T.);
#2627=ORIENTED_EDGE('',*,*,#2014,.F.);
#2628=ORIENTED_EDGE('',*,*,#2011,.F.);
#3121=CYLINDRICAL_SURFACE('',#3567,0.320000000000037);
#3122=CYLINDRICAL_SURFACE('',#3570,0.600000000000069);
#3227=ADVANCED_FACE('',(#605),#3121,.F.);
#3228=ADVANCED_FACE('',(#606),#3122,.T.);
#3229=ADVANCED_FACE('',(#607,#381),#457,.T.);
#3230=ADVANCED_FACE('',(#608,#382),#458,.F.);
#3336=CLOSED_SHELL('',(#3227,#3228,#3229,#3230));
#3566=AXIS2_PLACEMENT_3D('',#5254,#4222,#4223);
#3567=AXIS2_PLACEMENT_3D('',#5255,#4224,#4225);
#3568=AXIS2_PLACEMENT_3D('',#5257,#4226,#4227);
#3569=AXIS2_PLACEMENT_3D('',#5260,#4229,#4230);
#3570=AXIS2_PLACEMENT_3D('',#5261,#4231,#4232);
#3571=AXIS2_PLACEMENT_3D('',#5263,#4233,#4234);
#3572=AXIS2_PLACEMENT_3D('',#5266,#4236,#4237);
#3573=AXIS2_PLACEMENT_3D('',#5267,#4238,#4239);
#3574=AXIS2_PLACEMENT_3D('',#5268,#4240,#4241);
#4222=DIRECTION('axis',(0.,0.,1.));
#4223=DIRECTION('refdir',(1.,0.,0.));
#4224=DIRECTION('center_axis',(-6.12323399573548E-17,1.,4.78224871431377E-30));
#4225=DIRECTION('ref_axis',(0.939692587475203,5.75395759716863E-17,0.342020234846066));
#4226=DIRECTION('center_axis',(6.12323399573548E-17,-1.,-4.78224871431377E-30));
#4227=DIRECTION('ref_axis',(0.939692587475203,5.75395759716863E-17,0.342020234846066));
#4228=DIRECTION('',(6.12323399573548E-17,-1.,-4.78224871431377E-30));
#4229=DIRECTION('center_axis',(6.12323399573548E-17,-1.,-4.78224871431377E-30));
#4230=DIRECTION('ref_axis',(0.939692587475203,5.75395759716863E-17,0.342020234846066));
#4231=DIRECTION('center_axis',(-6.12323399573548E-17,1.,4.78224871431377E-30));
#4232=DIRECTION('ref_axis',(0.939692587475203,5.75395759716863E-17,0.342020234846066));
#4233=DIRECTION('center_axis',(-6.12323399573548E-17,1.,4.78224871431377E-30));
#4234=DIRECTION('ref_axis',(0.939692587475203,5.75395759716863E-17,0.342020234846066));
#4235=DIRECTION('',(6.12323399573548E-17,-1.,-4.78224871431377E-30));
#4236=DIRECTION('center_axis',(-6.12323399573548E-17,1.,4.78224871431377E-30));
#4237=DIRECTION('ref_axis',(0.939692587475203,5.75395759716863E-17,0.342020234846066));
#4238=DIRECTION('center_axis',(-6.12323399573548E-17,1.,4.78224871431377E-30));
#4239=DIRECTION('ref_axis',(0.939692587475203,5.75395759716863E-17,0.342020234846066));
#4240=DIRECTION('center_axis',(-6.12323399573548E-17,1.,4.78224871431377E-30));
#4241=DIRECTION('ref_axis',(0.939692587475203,5.75395759716863E-17,0.342020234846066));
#5254=CARTESIAN_POINT('',(0.,0.,0.));
#5255=CARTESIAN_POINT('Origin',(2.34923146868827,-1.72,3.85505058711526));
#5256=CARTESIAN_POINT('',(2.04852984069618,-1.55999999999998,3.74560411196451));
#5257=CARTESIAN_POINT('Origin',(2.34923146868827,-1.55999999999998,3.85505058711526));
#5258=CARTESIAN_POINT('',(2.04852984069618,-1.72,3.74560411196451));
#5259=CARTESIAN_POINT('',(2.04852984069618,-1.72,3.74560411196451));
#5260=CARTESIAN_POINT('Origin',(2.34923146868827,-1.72,3.85505058711526));
#5261=CARTESIAN_POINT('Origin',(2.34923146868827,-1.72,3.85505058711526));
#5262=CARTESIAN_POINT('',(1.78541591620309,-1.55999999999998,3.6498384462076));
#5263=CARTESIAN_POINT('Origin',(2.34923146868827,-1.55999999999998,3.85505058711526));
#5264=CARTESIAN_POINT('',(1.78541591620309,-1.72,3.6498384462076));
#5265=CARTESIAN_POINT('',(1.78541591620309,-1.72,3.6498384462076));
#5266=CARTESIAN_POINT('Origin',(2.34923146868827,-1.72,3.85505058711526));
#5267=CARTESIAN_POINT('Origin',(2.34923146868827,-1.55999999999998,3.85505058711526));
#5268=CARTESIAN_POINT('Origin',(2.34923146868827,-1.72,3.85505058711526));
#5890=UNCERTAINTY_MEASURE_WITH_UNIT(LENGTH_MEASURE(0.001),#5930,
'DISTANCE_ACCURACY_VALUE',
'Maximum model space distance between geometric entities at asserted c
onnectivities');
#5905=UNCERTAINTY_MEASURE_WITH_UNIT(LENGTH_MEASURE(0.001),#5930,
'DISTANCE_ACCURACY_VALUE',
'Maximum model space distance between geometric entities at asserted c
onnectivities');
#5914=(
GEOMETRIC_REPRESENTATION_CONTEXT(3)
GLOBAL_UNCERTAINTY_ASSIGNED_CONTEXT((#5890))
GLOBAL_UNIT_ASSIGNED_CONTEXT((#5930,#5932,#5933))
REPRESENTATION_CONTEXT('','3D')
);
#5929=(
GEOMETRIC_REPRESENTATION_CONTEXT(3)
GLOBAL_UNCERTAINTY_ASSIGNED_CONTEXT((#5905))
GLOBAL_UNIT_ASSIGNED_CONTEXT((#5930,#5932,#5933))
REPRESENTATION_CONTEXT('','3D')
);
#5930=(
LENGTH_UNIT()
NAMED_UNIT(*)
SI_UNIT(.CENTI.,.METRE.)
);
#5932=(
NAMED_UNIT(*)
PLANE_ANGLE_UNIT()
SI_UNIT($,.RADIAN.)
);
#5933=(
NAMED_UNIT(*)
SI_UNIT($,.STERADIAN.)
SOLID_ANGLE_UNIT()
);
#5942=SHAPE_DEFINITION_REPRESENTATION(#5965,#6047);
#5965=PRODUCT_DEFINITION_SHAPE('',$,#6071);
#6047=SHAPE_REPRESENTATION('',(#3566),#5914);
#6062=PRODUCT_DEFINITION_CONTEXT('part definition',#6133,'design');
#6071=PRODUCT_DEFINITION('Flat Washer - M6','Flat Washer - M6',#6094,
#6062);
#6094=PRODUCT_DEFINITION_FORMATION('',$,#6143);
#6133=APPLICATION_CONTEXT(
'Core Data for Automotive Mechanical Design Process');
#6134=PRODUCT_CONTEXT('part definition',#6133,'mechanical');
#6143=PRODUCT('Flat Washer - M6','Flat Washer - M6',
'Flat Washer - M6',(#6134));
#6221=COLOUR_RGB('Black',0.12,0.14,0.17);
#6222=FILL_AREA_STYLE_COLOUR('',#6221);
#6223=FILL_AREA_STYLE('',(#6222));
#6224=SURFACE_STYLE_FILL_AREA(#6223);
#6225=SURFACE_SIDE_STYLE('',(#6224));
#6226=SURFACE_STYLE_USAGE(.BOTH.,#6225);
#6227=PRESENTATION_STYLE_ASSIGNMENT((#6226));
ENDSEC;
END-ISO-10303-21;
